ISO-10303-21;
HEADER;
/* Generated by software containing ST-Developer
 * from STEP Tools, Inc. (www.steptools.com) 
 */

FILE_DESCRIPTION(
/* description */ (''),
/* implementation_level */ '2;1');

FILE_NAME(
/* name */ 'Screw.step',
/* time_stamp */ '2026-10-04T15:18:51-07:00',
/* author */ (''),
/* organization */ (''),
/* preprocessor_version */ 'ST-DEVELOPER v20.2',
/* originating_system */ 'Autodesk Translation Framework v15.15.0.0',
/* authorisation */ '');

FILE_SCHEMA (('AUTOMOTIVE_DESIGN { 1 0 10303 214 3 1 1 }'));
ENDSEC;

DATA;
#10=MECHANICAL_DESIGN_GEOMETRIC_PRESENTATION_REPRESENTATION('',(#72),#9891);
#43=B_SPLINE_CURVE_WITH_KNOTS('',3,(#8377,#8378,#8379,#8380,#8381,#8382,
#8383,#8384,#8385,#8386),.UNSPECIFIED.,.F.,.F.,(4,2,2,2,4),(0.015426059292352,
0.0589123817488116,0.11818030974329,0.178151638879277,0.239555012786688),
 .UNSPECIFIED.);
#44=B_SPLINE_CURVE_WITH_KNOTS('',3,(#8390,#8391,#8392,#8393,#8394,#8395,
#8396,#8397,#8398,#8399),.UNSPECIFIED.,.F.,.F.,(4,2,2,2,4),(0.740987738910849,
0.802391112818259,0.862362441954247,0.921630369948725,0.965116692405185),
 .UNSPECIFIED.);
#45=B_SPLINE_CURVE_WITH_KNOTS('',3,(#8404,#8405,#8406,#8407,#8408,#8409,
#8410,#8411,#8412,#8413),.UNSPECIFIED.,.F.,.F.,(4,2,2,2,4),(0.740987738910849,
0.80239111281826,0.862362441954247,0.921630369948725,0.965116692405185),
 .UNSPECIFIED.);
#46=B_SPLINE_CURVE_WITH_KNOTS('',3,(#8417,#8418,#8419,#8420,#8421,#8422,
#8423,#8424,#8425,#8426),.UNSPECIFIED.,.F.,.F.,(4,2,2,2,4),(0.015426059292352,
0.0589123817488117,0.11818030974329,0.178151638879277,0.239555012786688),
 .UNSPECIFIED.);
#53=SHAPE_REPRESENTATION_RELATIONSHIP('SRR','None',#9924,#61);
#61=ADVANCED_BREP_SHAPE_REPRESENTATION('',(#86),#9884);
#72=STYLED_ITEM('',(#9973),#86);
#86=MANIFOLD_SOLID_BREP('Body1',#5620);
#114=FACE_BOUND('',#825,.T.);
#179=PLANE('',#5867);
#180=PLANE('',#5868);
#181=PLANE('',#5869);
#182=PLANE('',#5873);
#183=PLANE('',#5875);
#184=PLANE('',#5882);
#185=PLANE('',#5883);
#357=TOROIDAL_SURFACE('',#5877,2.32389732910985,1.6);
#392=CONICAL_SURFACE('',#5864,1.8052925,0.829871117430571);
#393=CONICAL_SURFACE('',#5880,3.8950136037689,0.0872664625996596);
#394=CONICAL_SURFACE('',#5887,1.89262500000135,0.523598775596927);
#467=FACE_OUTER_BOUND('',#815,.T.);
#468=FACE_OUTER_BOUND('',#816,.T.);
#469=FACE_OUTER_BOUND('',#817,.T.);
#470=FACE_OUTER_BOUND('',#818,.T.);
#471=FACE_OUTER_BOUND('',#819,.T.);
#472=FACE_OUTER_BOUND('',#820,.T.);
#473=FACE_OUTER_BOUND('',#821,.T.);
#474=FACE_OUTER_BOUND('',#822,.T.);
#475=FACE_OUTER_BOUND('',#823,.T.);
#476=FACE_OUTER_BOUND('',#824,.T.);
#477=FACE_OUTER_BOUND('',#826,.T.);
#478=FACE_OUTER_BOUND('',#827,.T.);
#479=FACE_OUTER_BOUND('',#828,.T.);
#815=EDGE_LOOP('',(#3854,#3855,#3856,#3857));
#816=EDGE_LOOP('',(#3858,#3859,#3860,#3861));
#817=EDGE_LOOP('',(#3862,#3863,#3864,#3865));
#818=EDGE_LOOP('',(#3866,#3867,#3868,#3869,#3870));
#819=EDGE_LOOP('',(#3871,#3872));
#820=EDGE_LOOP('',(#3873,#3874));
#821=EDGE_LOOP('',(#3875,#3876,#3877,#3878,#3879,#3880,#3881,#3882,#3883,
#3884,#3885,#3886));
#822=EDGE_LOOP('',(#3887,#3888,#3889,#3890));
#823=EDGE_LOOP('',(#3891));
#824=EDGE_LOOP('',(#3892));
#825=EDGE_LOOP('',(#3893));
#826=EDGE_LOOP('',(#3894,#3895,#3896,#3897));
#827=EDGE_LOOP('',(#3898,#3899,#3900,#3901));
#828=EDGE_LOOP('',(#3902,#3903,#3904,#3905));
#1154=LINE('',#8372,#1618);
#1155=LINE('',#8388,#1619);
#1156=LINE('',#8400,#1620);
#1157=LINE('',#8415,#1621);
#1158=LINE('',#8427,#1622);
#1159=LINE('',#8444,#1623);
#1160=LINE('',#8452,#1624);
#1161=LINE('',#8456,#1625);
#1162=LINE('',#8458,#1626);
#1618=VECTOR('',#6687,1.8052925);
#1619=VECTOR('',#6692,10.);
#1620=VECTOR('',#6693,10.);
#1621=VECTOR('',#6696,10.);
#1622=VECTOR('',#6697,10.);
#1623=VECTOR('',#6724,3.8950136037689);
#1624=VECTOR('',#6735,1.78525000000062);
#1625=VECTOR('',#6740,1.89262500000135);
#1626=VECTOR('',#6743,1.954);
#2142=CIRCLE('',#5865,1.954);
#2143=CIRCLE('',#5866,1.570585);
#2144=CIRCLE('',#5870,3.91587722848039);
#2145=CIRCLE('',#5871,3.91587722848039);
#2146=CIRCLE('',#5872,3.91587722848039);
#2147=CIRCLE('',#5874,2.32389732910985);
#2148=CIRCLE('',#5876,2.32389732910985);
#2149=CIRCLE('',#5878,3.91780884605665);
#2150=CIRCLE('',#5879,1.6);
#2151=CIRCLE('',#5881,4.);
#2152=CIRCLE('',#5884,1.78524999999977);
#2153=CIRCLE('',#5886,1.78525000000146);
#2154=CIRCLE('',#5888,1.954);
#2427=VERTEX_POINT('',#8369);
#2428=VERTEX_POINT('',#8371);
#2429=VERTEX_POINT('',#8375);
#2430=VERTEX_POINT('',#8376);
#2431=VERTEX_POINT('',#8387);
#2432=VERTEX_POINT('',#8389);
#2433=VERTEX_POINT('',#8402);
#2434=VERTEX_POINT('',#8403);
#2435=VERTEX_POINT('',#8414);
#2436=VERTEX_POINT('',#8416);
#2437=VERTEX_POINT('',#8430);
#2438=VERTEX_POINT('',#8438);
#2439=VERTEX_POINT('',#8442);
#2440=VERTEX_POINT('',#8447);
#2441=VERTEX_POINT('',#8450);
#2442=VERTEX_POINT('',#8454);
#2972=EDGE_CURVE('',#2427,#2427,#2142,.T.);
#2973=EDGE_CURVE('',#2427,#2428,#1154,.T.);
#2974=EDGE_CURVE('',#2428,#2428,#2143,.T.);
#2975=EDGE_CURVE('',#2429,#2430,#43,.T.);
#2976=EDGE_CURVE('',#2429,#2431,#1155,.T.);
#2977=EDGE_CURVE('',#2432,#2431,#44,.T.);
#2978=EDGE_CURVE('',#2430,#2432,#1156,.T.);
#2979=EDGE_CURVE('',#2433,#2434,#45,.T.);
#2980=EDGE_CURVE('',#2435,#2433,#1157,.T.);
#2981=EDGE_CURVE('',#2436,#2435,#46,.T.);
#2982=EDGE_CURVE('',#2436,#2434,#1158,.T.);
#2983=EDGE_CURVE('',#2434,#2429,#2144,.T.);
#2984=EDGE_CURVE('',#2437,#2436,#2145,.T.);
#2985=EDGE_CURVE('',#2431,#2437,#2146,.T.);
#2986=EDGE_CURVE('',#2435,#2433,#2147,.T.);
#2987=EDGE_CURVE('',#2430,#2432,#2148,.T.);
#2988=EDGE_CURVE('',#2438,#2438,#2149,.T.);
#2989=EDGE_CURVE('',#2438,#2437,#2150,.T.);
#2990=EDGE_CURVE('',#2439,#2439,#2151,.T.);
#2991=EDGE_CURVE('',#2439,#2438,#1159,.T.);
#2992=EDGE_CURVE('',#2440,#2440,#2152,.T.);
#2993=EDGE_CURVE('',#2441,#2441,#2153,.T.);
#2994=EDGE_CURVE('',#2441,#2440,#1160,.T.);
#2995=EDGE_CURVE('',#2442,#2442,#2154,.T.);
#2996=EDGE_CURVE('',#2442,#2441,#1161,.T.);
#2997=EDGE_CURVE('',#2427,#2442,#1162,.T.);
#3854=ORIENTED_EDGE('',*,*,#2972,.F.);
#3855=ORIENTED_EDGE('',*,*,#2973,.T.);
#3856=ORIENTED_EDGE('',*,*,#2974,.F.);
#3857=ORIENTED_EDGE('',*,*,#2973,.F.);
#3858=ORIENTED_EDGE('',*,*,#2975,.F.);
#3859=ORIENTED_EDGE('',*,*,#2976,.T.);
#3860=ORIENTED_EDGE('',*,*,#2977,.F.);
#3861=ORIENTED_EDGE('',*,*,#2978,.F.);
#3862=ORIENTED_EDGE('',*,*,#2979,.F.);
#3863=ORIENTED_EDGE('',*,*,#2980,.F.);
#3864=ORIENTED_EDGE('',*,*,#2981,.F.);
#3865=ORIENTED_EDGE('',*,*,#2982,.T.);
#3866=ORIENTED_EDGE('',*,*,#2983,.F.);
#3867=ORIENTED_EDGE('',*,*,#2982,.F.);
#3868=ORIENTED_EDGE('',*,*,#2984,.F.);
#3869=ORIENTED_EDGE('',*,*,#2985,.F.);
#3870=ORIENTED_EDGE('',*,*,#2976,.F.);
#3871=ORIENTED_EDGE('',*,*,#2980,.T.);
#3872=ORIENTED_EDGE('',*,*,#2986,.F.);
#3873=ORIENTED_EDGE('',*,*,#2978,.T.);
#3874=ORIENTED_EDGE('',*,*,#2987,.F.);
#3875=ORIENTED_EDGE('',*,*,#2988,.T.);
#3876=ORIENTED_EDGE('',*,*,#2989,.T.);
#3877=ORIENTED_EDGE('',*,*,#2984,.T.);
#3878=ORIENTED_EDGE('',*,*,#2981,.T.);
#3879=ORIENTED_EDGE('',*,*,#2986,.T.);
#3880=ORIENTED_EDGE('',*,*,#2979,.T.);
#3881=ORIENTED_EDGE('',*,*,#2983,.T.);
#3882=ORIENTED_EDGE('',*,*,#2975,.T.);
#3883=ORIENTED_EDGE('',*,*,#2987,.T.);
#3884=ORIENTED_EDGE('',*,*,#2977,.T.);
#3885=ORIENTED_EDGE('',*,*,#2985,.T.);
#3886=ORIENTED_EDGE('',*,*,#2989,.F.);
#3887=ORIENTED_EDGE('',*,*,#2990,.F.);
#3888=ORIENTED_EDGE('',*,*,#2991,.T.);
#3889=ORIENTED_EDGE('',*,*,#2988,.F.);
#3890=ORIENTED_EDGE('',*,*,#2991,.F.);
#3891=ORIENTED_EDGE('',*,*,#2974,.T.);
#3892=ORIENTED_EDGE('',*,*,#2990,.T.);
#3893=ORIENTED_EDGE('',*,*,#2992,.F.);
#3894=ORIENTED_EDGE('',*,*,#2993,.F.);
#3895=ORIENTED_EDGE('',*,*,#2994,.T.);
#3896=ORIENTED_EDGE('',*,*,#2992,.T.);
#3897=ORIENTED_EDGE('',*,*,#2994,.F.);
#3898=ORIENTED_EDGE('',*,*,#2995,.F.);
#3899=ORIENTED_EDGE('',*,*,#2996,.T.);
#3900=ORIENTED_EDGE('',*,*,#2993,.T.);
#3901=ORIENTED_EDGE('',*,*,#2996,.F.);
#3902=ORIENTED_EDGE('',*,*,#2972,.T.);
#3903=ORIENTED_EDGE('',*,*,#2997,.T.);
#3904=ORIENTED_EDGE('',*,*,#2995,.T.);
#3905=ORIENTED_EDGE('',*,*,#2997,.F.);
#5212=CYLINDRICAL_SURFACE('',#5885,1.78525000000062);
#5213=CYLINDRICAL_SURFACE('',#5889,1.954);
#5346=ADVANCED_FACE('',(#467),#392,.T.);
#5347=ADVANCED_FACE('',(#468),#179,.F.);
#5348=ADVANCED_FACE('',(#469),#180,.F.);
#5349=ADVANCED_FACE('',(#470),#181,.T.);
#5350=ADVANCED_FACE('',(#471),#182,.T.);
#5351=ADVANCED_FACE('',(#472),#183,.T.);
#5352=ADVANCED_FACE('',(#473),#357,.T.);
#5353=ADVANCED_FACE('',(#474),#393,.T.);
#5354=ADVANCED_FACE('',(#475),#184,.T.);
#5355=ADVANCED_FACE('',(#476,#114),#185,.T.);
#5356=ADVANCED_FACE('',(#477),#5212,.T.);
#5357=ADVANCED_FACE('',(#478),#394,.T.);
#5358=ADVANCED_FACE('',(#479),#5213,.T.);
#5620=CLOSED_SHELL('',(#5346,#5347,#5348,#5349,#5350,#5351,#5352,#5353,
#5354,#5355,#5356,#5357,#5358));
#5863=AXIS2_PLACEMENT_3D('',#8367,#6681,#6682);
#5864=AXIS2_PLACEMENT_3D('',#8368,#6683,#6684);
#5865=AXIS2_PLACEMENT_3D('',#8370,#6685,#6686);
#5866=AXIS2_PLACEMENT_3D('',#8373,#6688,#6689);
#5867=AXIS2_PLACEMENT_3D('',#8374,#6690,#6691);
#5868=AXIS2_PLACEMENT_3D('',#8401,#6694,#6695);
#5869=AXIS2_PLACEMENT_3D('',#8428,#6698,#6699);
#5870=AXIS2_PLACEMENT_3D('',#8429,#6700,#6701);
#5871=AXIS2_PLACEMENT_3D('',#8431,#6702,#6703);
#5872=AXIS2_PLACEMENT_3D('',#8432,#6704,#6705);
#5873=AXIS2_PLACEMENT_3D('',#8433,#6706,#6707);
#5874=AXIS2_PLACEMENT_3D('',#8434,#6708,#6709);
#5875=AXIS2_PLACEMENT_3D('',#8435,#6710,#6711);
#5876=AXIS2_PLACEMENT_3D('',#8436,#6712,#6713);
#5877=AXIS2_PLACEMENT_3D('',#8437,#6714,#6715);
#5878=AXIS2_PLACEMENT_3D('',#8439,#6716,#6717);
#5879=AXIS2_PLACEMENT_3D('',#8440,#6718,#6719);
#5880=AXIS2_PLACEMENT_3D('',#8441,#6720,#6721);
#5881=AXIS2_PLACEMENT_3D('',#8443,#6722,#6723);
#5882=AXIS2_PLACEMENT_3D('',#8445,#6725,#6726);
#5883=AXIS2_PLACEMENT_3D('',#8446,#6727,#6728);
#5884=AXIS2_PLACEMENT_3D('',#8448,#6729,#6730);
#5885=AXIS2_PLACEMENT_3D('',#8449,#6731,#6732);
#5886=AXIS2_PLACEMENT_3D('',#8451,#6733,#6734);
#5887=AXIS2_PLACEMENT_3D('',#8453,#6736,#6737);
#5888=AXIS2_PLACEMENT_3D('',#8455,#6738,#6739);
#5889=AXIS2_PLACEMENT_3D('',#8457,#6741,#6742);
#6681=DIRECTION('axis',(0.,0.,1.));
#6682=DIRECTION('refdir',(1.,0.,0.));
#6683=DIRECTION('center_axis',(0.,0.,1.));
#6684=DIRECTION('ref_axis',(-1.,0.,0.));
#6685=DIRECTION('center_axis',(-1.22514845490924E-16,0.,1.));
#6686=DIRECTION('ref_axis',(-1.,0.,-1.22514845490924E-16));
#6687=DIRECTION('',(-0.737844385259416,-9.0359876467679E-17,-0.67497086095709));
#6688=DIRECTION('center_axis',(1.22514845490924E-16,0.,-1.));
#6689=DIRECTION('ref_axis',(-1.,0.,-1.22514845490924E-16));
#6690=DIRECTION('center_axis',(-8.67361737988404E-17,1.,0.));
#6691=DIRECTION('ref_axis',(1.,8.67361737988404E-17,0.));
#6692=DIRECTION('',(1.,8.67361737988404E-17,0.));
#6693=DIRECTION('',(1.,8.67361737988404E-17,1.22514845490924E-16));
#6694=DIRECTION('center_axis',(1.64798730217797E-16,-1.,0.));
#6695=DIRECTION('ref_axis',(-1.,-1.64798730217797E-16,0.));
#6696=DIRECTION('',(-1.,-1.64798730217797E-16,-1.22514845490924E-16));
#6697=DIRECTION('',(-1.,-1.64798730217797E-16,0.));
#6698=DIRECTION('center_axis',(0.,0.,1.));
#6699=DIRECTION('ref_axis',(1.,0.,0.));
#6700=DIRECTION('center_axis',(6.12574227454618E-17,0.,-1.));
#6701=DIRECTION('ref_axis',(-1.,0.,-6.12574227454618E-17));
#6702=DIRECTION('center_axis',(6.12574227454618E-17,0.,-1.));
#6703=DIRECTION('ref_axis',(-1.,0.,-6.12574227454618E-17));
#6704=DIRECTION('center_axis',(6.12574227454618E-17,0.,-1.));
#6705=DIRECTION('ref_axis',(-1.,0.,-6.12574227454618E-17));
#6706=DIRECTION('center_axis',(-1.22514845490924E-16,0.,1.));
#6707=DIRECTION('ref_axis',(1.,0.,1.22514845490924E-16));
#6708=DIRECTION('center_axis',(1.22514845490924E-16,0.,-1.));
#6709=DIRECTION('ref_axis',(1.,0.,1.22514845490924E-16));
#6710=DIRECTION('center_axis',(-1.22514845490924E-16,0.,1.));
#6711=DIRECTION('ref_axis',(1.,0.,1.22514845490924E-16));
#6712=DIRECTION('center_axis',(1.22514845490924E-16,0.,-1.));
#6713=DIRECTION('ref_axis',(1.,0.,1.22514845490924E-16));
#6714=DIRECTION('center_axis',(1.22514845490924E-16,0.,-1.));
#6715=DIRECTION('ref_axis',(-1.,0.,-1.41469428416086E-16));
#6716=DIRECTION('center_axis',(-1.41689279422427E-16,1.28384806450313E-32,
1.));
#6717=DIRECTION('ref_axis',(1.,-6.12323399573677E-17,1.41689279422427E-16));
#6718=DIRECTION('center_axis',(-1.22464679914735E-16,-1.,-1.50037413378493E-32));
#6719=DIRECTION('ref_axis',(1.,-1.22464679914735E-16,1.06102071312065E-16));
#6720=DIRECTION('center_axis',(1.22514845490924E-16,0.,-1.));
#6721=DIRECTION('ref_axis',(-1.,0.,-1.22514845490924E-16));
#6722=DIRECTION('center_axis',(1.22514845490924E-16,0.,-1.));
#6723=DIRECTION('ref_axis',(1.,0.,1.22514845490924E-16));
#6724=DIRECTION('',(-0.0871557427476016,1.0673500138316E-17,0.99619469809175));
#6725=DIRECTION('center_axis',(1.22514845490924E-16,0.,-1.));
#6726=DIRECTION('ref_axis',(-1.,0.,-1.22514845490924E-16));
#6727=DIRECTION('center_axis',(1.22514845490924E-16,0.,-1.));
#6728=DIRECTION('ref_axis',(-1.,0.,-1.22514845490924E-16));
#6729=DIRECTION('center_axis',(1.22514845490924E-16,0.,-1.));
#6730=DIRECTION('ref_axis',(1.,0.,1.22514845490924E-16));
#6731=DIRECTION('center_axis',(1.22514845490924E-16,0.,-1.));
#6732=DIRECTION('ref_axis',(-1.,0.,-1.22514845490924E-16));
#6733=DIRECTION('center_axis',(1.22514845490924E-16,0.,-1.));
#6734=DIRECTION('ref_axis',(1.,0.,1.22514845490924E-16));
#6735=DIRECTION('',(-1.22514845490924E-16,0.,1.));
#6736=DIRECTION('center_axis',(1.22514845490924E-16,0.,-1.));
#6737=DIRECTION('ref_axis',(-1.,0.,-1.22514845490924E-16));
#6738=DIRECTION('center_axis',(1.22514845490924E-16,0.,-1.));
#6739=DIRECTION('ref_axis',(-1.,0.,-1.22514845490924E-16));
#6740=DIRECTION('',(-0.499999999998812,6.12323399572222E-17,0.866025403785125));
#6741=DIRECTION('center_axis',(1.22514845490924E-16,0.,-1.));
#6742=DIRECTION('ref_axis',(-1.,0.,-1.22514845490924E-16));
#6743=DIRECTION('',(-1.22514845490924E-16,0.,1.));
#8367=CARTESIAN_POINT('',(0.,0.,0.));
#8368=CARTESIAN_POINT('Origin',(0.,0.,-5.78529249999847));
#8369=CARTESIAN_POINT('',(1.954,2.39295984553393E-16,-5.64925672970459));
#8370=CARTESIAN_POINT('Origin',(6.92117815378051E-16,0.,-5.64925672970459));
#8371=CARTESIAN_POINT('',(1.570585,-1.92341189303885E-16,-5.99999999999847));
#8372=CARTESIAN_POINT('',(1.8052925,2.21084568164972E-16,-5.78529249999847));
#8373=CARTESIAN_POINT('Origin',(0.,0.,-5.99999999999847));
#8374=CARTESIAN_POINT('Origin',(-3.95474398665704,0.6,2.4));
#8375=CARTESIAN_POINT('',(-3.86963751125752,0.6,0.96));
#8376=CARTESIAN_POINT('',(-2.24510552006891,0.6,2.4));
#8377=CARTESIAN_POINT('Ctrl Pts',(-3.86963751125752,0.6,0.96));
#8378=CARTESIAN_POINT('Ctrl Pts',(-3.85395158312663,0.6,1.11423006273542));
#8379=CARTESIAN_POINT('Ctrl Pts',(-3.81170536802524,0.6,1.27490216957991));
#8380=CARTESIAN_POINT('Ctrl Pts',(-3.67998890871741,0.6,1.59107732632764));
#8381=CARTESIAN_POINT('Ctrl Pts',(-3.54752952367749,0.6,1.78769245274213));
#8382=CARTESIAN_POINT('Ctrl Pts',(-3.26545084874928,0.6,2.06770924479005));
#8383=CARTESIAN_POINT('Ctrl Pts',(-3.06525849356145,0.6,2.19987575347413));
#8384=CARTESIAN_POINT('Ctrl Pts',(-2.69093530578108,0.6,2.35339781620156));
#8385=CARTESIAN_POINT('Ctrl Pts',(-2.44978343309361,0.6,2.39999999999952));
#8386=CARTESIAN_POINT('Ctrl Pts',(-2.24510552006891,0.6,2.39999999999952));
#8387=CARTESIAN_POINT('',(3.86963751125752,0.600000000000001,0.96));
#8388=CARTESIAN_POINT('',(-4.,0.6,0.96));
#8389=CARTESIAN_POINT('',(2.24510552006891,0.6,2.4));
#8390=CARTESIAN_POINT('Ctrl Pts',(2.24510552006891,0.600000000000001,2.39999999999952));
#8391=CARTESIAN_POINT('Ctrl Pts',(2.44978343309361,0.600000000000001,2.39999999999952));
#8392=CARTESIAN_POINT('Ctrl Pts',(2.69093530578108,0.600000000000001,2.35339781620157));
#8393=CARTESIAN_POINT('Ctrl Pts',(3.06525849356145,0.600000000000001,2.19987575347413));
#8394=CARTESIAN_POINT('Ctrl Pts',(3.26545084874928,0.600000000000001,2.06770924479005));
#8395=CARTESIAN_POINT('Ctrl Pts',(3.54752952367749,0.600000000000001,1.78769245274213));
#8396=CARTESIAN_POINT('Ctrl Pts',(3.67998890871741,0.600000000000001,1.59107732632764));
#8397=CARTESIAN_POINT('Ctrl Pts',(3.81170536802524,0.600000000000001,1.27490216957991));
#8398=CARTESIAN_POINT('Ctrl Pts',(3.85395158312663,0.600000000000001,1.11423006273542));
#8399=CARTESIAN_POINT('Ctrl Pts',(3.86963751125752,0.600000000000001,0.96));
#8400=CARTESIAN_POINT('',(-3.87238559709742,0.6,2.39999999999952));
#8401=CARTESIAN_POINT('Origin',(3.95474398665704,-0.6,2.4));
#8402=CARTESIAN_POINT('',(-2.24510552006891,-0.600000000000001,2.4));
#8403=CARTESIAN_POINT('',(-3.86963751125752,-0.600000000000001,0.96));
#8404=CARTESIAN_POINT('Ctrl Pts',(-2.24510552006891,-0.600000000000001,
2.39999999999952));
#8405=CARTESIAN_POINT('Ctrl Pts',(-2.44978343309361,-0.600000000000001,
2.39999999999952));
#8406=CARTESIAN_POINT('Ctrl Pts',(-2.69093530578108,-0.600000000000001,
2.35339781620156));
#8407=CARTESIAN_POINT('Ctrl Pts',(-3.06525849356145,-0.600000000000001,
2.19987575347413));
#8408=CARTESIAN_POINT('Ctrl Pts',(-3.26545084874928,-0.600000000000001,
2.06770924479005));
#8409=CARTESIAN_POINT('Ctrl Pts',(-3.54752952367749,-0.600000000000001,
1.78769245274213));
#8410=CARTESIAN_POINT('Ctrl Pts',(-3.67998890871741,-0.600000000000001,
1.59107732632764));
#8411=CARTESIAN_POINT('Ctrl Pts',(-3.81170536802524,-0.600000000000001,
1.27490216957991));
#8412=CARTESIAN_POINT('Ctrl Pts',(-3.85395158312663,-0.600000000000001,
1.11423006273542));
#8413=CARTESIAN_POINT('Ctrl Pts',(-3.86963751125752,-0.600000000000001,
0.96));
#8414=CARTESIAN_POINT('',(2.24510552006891,-0.6,2.4));
#8415=CARTESIAN_POINT('',(0.0823583895596134,-0.6,2.39999999999952));
#8416=CARTESIAN_POINT('',(3.86963751125752,-0.6,0.96));
#8417=CARTESIAN_POINT('Ctrl Pts',(3.86963751125752,-0.6,0.96));
#8418=CARTESIAN_POINT('Ctrl Pts',(3.85395158312663,-0.6,1.11423006273542));
#8419=CARTESIAN_POINT('Ctrl Pts',(3.81170536802524,-0.6,1.27490216957991));
#8420=CARTESIAN_POINT('Ctrl Pts',(3.67998890871741,-0.6,1.59107732632764));
#8421=CARTESIAN_POINT('Ctrl Pts',(3.54752952367749,-0.6,1.78769245274213));
#8422=CARTESIAN_POINT('Ctrl Pts',(3.26545084874928,-0.6,2.06770924479005));
#8423=CARTESIAN_POINT('Ctrl Pts',(3.06525849356145,-0.6,2.19987575347413));
#8424=CARTESIAN_POINT('Ctrl Pts',(2.69093530578108,-0.6,2.35339781620157));
#8425=CARTESIAN_POINT('Ctrl Pts',(2.44978343309361,-0.6,2.39999999999952));
#8426=CARTESIAN_POINT('Ctrl Pts',(2.24510552006891,-0.6,2.39999999999952));
#8427=CARTESIAN_POINT('',(4.,-0.6,0.96));
#8428=CARTESIAN_POINT('Origin',(0.,0.,0.96));
#8429=CARTESIAN_POINT('Origin',(-1.0781306403225E-16,0.,0.96));
#8430=CARTESIAN_POINT('',(3.91587722848039,-4.79556651371252E-16,0.96));
#8431=CARTESIAN_POINT('Origin',(-1.0781306403225E-16,0.,0.96));
#8432=CARTESIAN_POINT('Origin',(-1.0781306403225E-16,0.,0.96));
#8433=CARTESIAN_POINT('Origin',(-3.79002720753781,0.,2.39999999999952));
#8434=CARTESIAN_POINT('Origin',(-2.94035629178425E-16,0.,2.39999999999952));
#8435=CARTESIAN_POINT('Origin',(-3.79002720753781,0.,2.39999999999952));
#8436=CARTESIAN_POINT('Origin',(-2.94035629178425E-16,0.,2.39999999999952));
#8437=CARTESIAN_POINT('Origin',(-9.80118763929471E-17,0.,0.799999999999521));
#8438=CARTESIAN_POINT('',(3.91780884605665,-4.79793206299446E-16,0.939449188395684));
#8439=CARTESIAN_POINT('Origin',(0.,-2.39896603149723E-16,0.939449188395683));
#8440=CARTESIAN_POINT('Origin',(2.32389732910985,-2.84595342564146E-16,
0.799999999999521));
#8441=CARTESIAN_POINT('Origin',(-1.4701781458924E-16,0.,1.1999999999989));
#8442=CARTESIAN_POINT('',(4.,-4.89858719658941E-16,-1.72986625024407E-12));
#8443=CARTESIAN_POINT('Origin',(-5.48504848161485E-29,0.,-1.72917236085368E-12));
#8444=CARTESIAN_POINT('',(3.8950136037689,-4.77001594249098E-16,1.1999999999989));
#8445=CARTESIAN_POINT('Origin',(8.32667268468867E-16,0.,-5.99999999999847));
#8446=CARTESIAN_POINT('Origin',(-1.78524999999977,0.,-7.71874504793049E-13));
#8447=CARTESIAN_POINT('',(1.78525000000062,-2.18630069817857E-16,-7.71535613175445E-13));
#8448=CARTESIAN_POINT('Origin',(-1.72131914709554E-28,0.,-7.71605002114484E-13));
#8449=CARTESIAN_POINT('Origin',(6.4320293882545E-17,0.,-0.525000000000627));
#8450=CARTESIAN_POINT('',(1.78525000000062,-2.18630069817857E-16,-1.05000000000048));
#8451=CARTESIAN_POINT('Origin',(1.28640587765262E-16,0.,-1.05000000000048));
#8452=CARTESIAN_POINT('',(1.78525000000062,-2.18630069817857E-16,-0.525000000000627));
#8453=CARTESIAN_POINT('Origin',(1.51425770758387E-16,0.,-1.23597895546358));
#8454=CARTESIAN_POINT('',(1.954,-2.39295984553393E-16,-1.34228357377612));
#8455=CARTESIAN_POINT('Origin',(1.64449664645919E-16,0.,-1.34228357377612));
#8456=CARTESIAN_POINT('',(1.89262500000135,-2.31779714823791E-16,-1.23597895546358));
#8457=CARTESIAN_POINT('Origin',(4.54650013348477E-16,0.,-3.71097895546402));
#8458=CARTESIAN_POINT('',(1.954,-2.39295984553393E-16,-3.71097895546402));
#9874=UNCERTAINTY_MEASURE_WITH_UNIT(LENGTH_MEASURE(0.01),#9892,
'DISTANCE_ACCURACY_VALUE',
'Maximum model space distance between geometric entities at asserted c
onnectivities');
#9881=UNCERTAINTY_MEASURE_WITH_UNIT(LENGTH_MEASURE(0.01),#9892,
'DISTANCE_ACCURACY_VALUE',
'Maximum model space distance between geometric entities at asserted c
onnectivities');
#9884=(
GEOMETRIC_REPRESENTATION_CONTEXT(3)
GLOBAL_UNCERTAINTY_ASSIGNED_CONTEXT((#9874))
GLOBAL_UNIT_ASSIGNED_CONTEXT((#9892,#9894,#9895))
REPRESENTATION_CONTEXT('','3D')
);
#9891=(
GEOMETRIC_REPRESENTATION_CONTEXT(3)
GLOBAL_UNCERTAINTY_ASSIGNED_CONTEXT((#9881))
GLOBAL_UNIT_ASSIGNED_CONTEXT((#9892,#9894,#9895))
REPRESENTATION_CONTEXT('','3D')
);
#9892=(
LENGTH_UNIT()
NAMED_UNIT(*)
SI_UNIT(.MILLI.,.METRE.)
);
#9894=(
NAMED_UNIT(*)
PLANE_ANGLE_UNIT()
SI_UNIT($,.RADIAN.)
);
#9895=(
NAMED_UNIT(*)
SI_UNIT($,.STERADIAN.)
SOLID_ANGLE_UNIT()
);
#9898=SHAPE_DEFINITION_REPRESENTATION(#9907,#9924);
#9907=PRODUCT_DEFINITION_SHAPE('',$,#9934);
#9924=SHAPE_REPRESENTATION('',(#5863),#9884);
#9931=PRODUCT_DEFINITION_CONTEXT('part definition',#9960,'design');
#9934=PRODUCT_DEFINITION('SPHS BS 4183 - M4 x 6 Steel 4.6 Plain',
'Screw',#9943,#9931);
#9943=PRODUCT_DEFINITION_FORMATION('',$,#9964);
#9960=APPLICATION_CONTEXT(
'Core Data for Automotive Mechanical Design Process');
#9961=PRODUCT_CONTEXT('part definition',#9960,'mechanical');
#9964=PRODUCT('SPHS BS 4183 - M4 x 6 Steel 4.6 Plain','Screw',
'Slotted Pan Head Screw BS 4183 - M4 x 6',(#9961));
#9973=PRESENTATION_STYLE_ASSIGNMENT((#9978));
#9978=SURFACE_STYLE_USAGE(.BOTH.,#9983);
#9983=SURFACE_SIDE_STYLE('',(#9988));
#9988=SURFACE_STYLE_FILL_AREA(#9993);
#9993=FILL_AREA_STYLE('Opaque(48,59,150)',(#9998));
#9998=FILL_AREA_STYLE_COLOUR('Opaque(48,59,150)',#10003);
#10003=COLOUR_RGB('Opaque(48,59,150)', 0.72549020, 0.75294118, 0.79215686);
ENDSEC;
END-ISO-10303-21;
